ISO-10303-21;
HEADER;
/* Generated by software containing ST-Developer
 * from STEP Tools, Inc. (www.steptools.com) 
 */

FILE_DESCRIPTION(
/* description */ ('STEP AP214'),
/* implementation_level */ '2;1');

FILE_NAME(
/* name */ 'Ball Screw Support Bracket.step',
/* time_stamp */ '2026-11-15T14:49:54-08:00',
/* author */ (''),
/* organization */ (''),
/* preprocessor_version */ 'ST-DEVELOPER v20.2',
/* originating_system */ 'Autodesk Translation Framework v15.17.0.0',
/* authorisation */ '');

FILE_SCHEMA (('AUTOMOTIVE_DESIGN { 1 0 10303 214 3 1 1 }'));
ENDSEC;

DATA;
#10=MECHANICAL_DESIGN_GEOMETRIC_PRESENTATION_REPRESENTATION('',(#1101),#66721);
#1039=SHAPE_REPRESENTATION_RELATIONSHIP('SRR','None',#66896,#1070);
#1070=ADVANCED_BREP_SHAPE_REPRESENTATION('',(#1136),#66687);
#1101=STYLED_ITEM('',(#67095),#1136);
#1136=MANIFOLD_SOLID_BREP('Body1',#25667);
#1209=FACE_BOUND('',#3815,.T.);
#1210=FACE_BOUND('',#3816,.T.);
#1211=FACE_BOUND('',#3817,.T.);
#1212=FACE_BOUND('',#3818,.T.);
#1213=FACE_BOUND('',#3819,.T.);
#1214=FACE_BOUND('',#3820,.T.);
#1215=FACE_BOUND('',#3821,.T.);
#1216=FACE_BOUND('',#3824,.T.);
#1217=FACE_BOUND('',#3825,.T.);
#1218=FACE_BOUND('',#3826,.T.);
#1219=FACE_BOUND('',#3827,.T.);
#1220=FACE_BOUND('',#3828,.T.);
#1221=FACE_BOUND('',#3829,.T.);
#1222=FACE_BOUND('',#3830,.T.);
#1533=PLANE('',#26164);
#1534=PLANE('',#26167);
#1535=PLANE('',#26168);
#1536=PLANE('',#26171);
#1537=PLANE('',#26172);
#1538=PLANE('',#26173);
#2324=FACE_OUTER_BOUND('',#3807,.T.);
#2325=FACE_OUTER_BOUND('',#3808,.T.);
#2326=FACE_OUTER_BOUND('',#3809,.T.);
#2327=FACE_OUTER_BOUND('',#3810,.T.);
#2328=FACE_OUTER_BOUND('',#3811,.T.);
#2329=FACE_OUTER_BOUND('',#3812,.T.);
#2330=FACE_OUTER_BOUND('',#3813,.T.);
#2331=FACE_OUTER_BOUND('',#3814,.T.);
#2332=FACE_OUTER_BOUND('',#3822,.T.);
#2333=FACE_OUTER_BOUND('',#3823,.T.);
#2334=FACE_OUTER_BOUND('',#3831,.T.);
#2335=FACE_OUTER_BOUND('',#3832,.T.);
#2336=FACE_OUTER_BOUND('',#3833,.T.);
#2337=FACE_OUTER_BOUND('',#3834,.T.);
#2338=FACE_OUTER_BOUND('',#3835,.T.);
#3807=EDGE_LOOP('',(#16870,#16871,#16872,#16873));
#3808=EDGE_LOOP('',(#16874,#16875,#16876,#16877));
#3809=EDGE_LOOP('',(#16878,#16879,#16880,#16881));
#3810=EDGE_LOOP('',(#16882,#16883,#16884,#16885));
#3811=EDGE_LOOP('',(#16886,#16887,#16888,#16889));
#3812=EDGE_LOOP('',(#16890,#16891,#16892,#16893));
#3813=EDGE_LOOP('',(#16894,#16895,#16896,#16897));
#3814=EDGE_LOOP('',(#16898,#16899,#16900,#16901,#16902,#16903));
#3815=EDGE_LOOP('',(#16904));
#3816=EDGE_LOOP('',(#16905));
#3817=EDGE_LOOP('',(#16906));
#3818=EDGE_LOOP('',(#16907));
#3819=EDGE_LOOP('',(#16908));
#3820=EDGE_LOOP('',(#16909));
#3821=EDGE_LOOP('',(#16910));
#3822=EDGE_LOOP('',(#16911,#16912,#16913,#16914));
#3823=EDGE_LOOP('',(#16915,#16916,#16917,#16918,#16919,#16920));
#3824=EDGE_LOOP('',(#16921));
#3825=EDGE_LOOP('',(#16922));
#3826=EDGE_LOOP('',(#16923));
#3827=EDGE_LOOP('',(#16924));
#3828=EDGE_LOOP('',(#16925));
#3829=EDGE_LOOP('',(#16926));
#3830=EDGE_LOOP('',(#16927));
#3831=EDGE_LOOP('',(#16928,#16929,#16930,#16931));
#3832=EDGE_LOOP('',(#16932,#16933,#16934,#16935));
#3833=EDGE_LOOP('',(#16936,#16937,#16938,#16939));
#3834=EDGE_LOOP('',(#16940,#16941,#16942,#16943));
#3835=EDGE_LOOP('',(#16944,#16945,#16946,#16947));
#5581=LINE('',#36471,#7570);
#5582=LINE('',#36477,#7571);
#5583=LINE('',#36483,#7572);
#5584=LINE('',#36489,#7573);
#5585=LINE('',#36495,#7574);
#5586=LINE('',#36501,#7575);
#5587=LINE('',#36507,#7576);
#5588=LINE('',#36512,#7577);
#5589=LINE('',#36516,#7578);
#5590=LINE('',#36518,#7579);
#5591=LINE('',#36520,#7580);
#5592=LINE('',#36525,#7581);
#5593=LINE('',#36526,#7582);
#5594=LINE('',#36527,#7583);
#5595=LINE('',#36531,#7584);
#5596=LINE('',#36536,#7585);
#5597=LINE('',#36537,#7586);
#5598=LINE('',#36539,#7587);
#5599=LINE('',#36540,#7588);
#5600=LINE('',#36542,#7589);
#5601=LINE('',#36544,#7590);
#7570=VECTOR('',#29062,2.1);
#7571=VECTOR('',#29069,2.1);
#7572=VECTOR('',#29076,2.1);
#7573=VECTOR('',#29083,2.1);
#7574=VECTOR('',#29090,2.1);
#7575=VECTOR('',#29097,2.1);
#7576=VECTOR('',#29104,18.);
#7577=VECTOR('',#29109,1000.);
#7578=VECTOR('',#29112,1000.);
#7579=VECTOR('',#29113,1000.);
#7580=VECTOR('',#29114,1000.);
#7581=VECTOR('',#29119,1000.);
#7582=VECTOR('',#29120,1000.);
#7583=VECTOR('',#29121,1000.);
#7584=VECTOR('',#29124,1000.);
#7585=VECTOR('',#29129,1000.);
#7586=VECTOR('',#29130,1000.);
#7587=VECTOR('',#29133,1000.);
#7588=VECTOR('',#29134,1000.);
#7589=VECTOR('',#29137,1000.);
#7590=VECTOR('',#29140,1000.);
#9501=CIRCLE('',#26144,2.1);
#9502=CIRCLE('',#26145,2.1);
#9503=CIRCLE('',#26147,2.1);
#9504=CIRCLE('',#26148,2.1);
#9505=CIRCLE('',#26150,2.1);
#9506=CIRCLE('',#26151,2.1);
#9507=CIRCLE('',#26153,2.1);
#9508=CIRCLE('',#26154,2.1);
#9509=CIRCLE('',#26156,2.1);
#9510=CIRCLE('',#26157,2.1);
#9511=CIRCLE('',#26159,2.1);
#9512=CIRCLE('',#26160,2.1);
#9513=CIRCLE('',#26162,18.);
#9514=CIRCLE('',#26163,18.);
#9515=CIRCLE('',#26165,10.);
#9516=CIRCLE('',#26166,10.);
#9517=CIRCLE('',#26169,10.);
#9518=CIRCLE('',#26170,10.);
#10730=VERTEX_POINT('',#36468);
#10731=VERTEX_POINT('',#36470);
#10732=VERTEX_POINT('',#36474);
#10733=VERTEX_POINT('',#36476);
#10734=VERTEX_POINT('',#36480);
#10735=VERTEX_POINT('',#36482);
#10736=VERTEX_POINT('',#36486);
#10737=VERTEX_POINT('',#36488);
#10738=VERTEX_POINT('',#36492);
#10739=VERTEX_POINT('',#36494);
#10740=VERTEX_POINT('',#36498);
#10741=VERTEX_POINT('',#36500);
#10742=VERTEX_POINT('',#36504);
#10743=VERTEX_POINT('',#36506);
#10744=VERTEX_POINT('',#36510);
#10745=VERTEX_POINT('',#36511);
#10746=VERTEX_POINT('',#36513);
#10747=VERTEX_POINT('',#36515);
#10748=VERTEX_POINT('',#36517);
#10749=VERTEX_POINT('',#36519);
#10750=VERTEX_POINT('',#36523);
#10751=VERTEX_POINT('',#36524);
#10752=VERTEX_POINT('',#36529);
#10753=VERTEX_POINT('',#36530);
#10754=VERTEX_POINT('',#36533);
#10755=VERTEX_POINT('',#36535);
#13128=EDGE_CURVE('',#10730,#10730,#9501,.T.);
#13129=EDGE_CURVE('',#10730,#10731,#5581,.T.);
#13130=EDGE_CURVE('',#10731,#10731,#9502,.T.);
#13131=EDGE_CURVE('',#10732,#10732,#9503,.T.);
#13132=EDGE_CURVE('',#10732,#10733,#5582,.T.);
#13133=EDGE_CURVE('',#10733,#10733,#9504,.T.);
#13134=EDGE_CURVE('',#10734,#10734,#9505,.T.);
#13135=EDGE_CURVE('',#10734,#10735,#5583,.T.);
#13136=EDGE_CURVE('',#10735,#10735,#9506,.T.);
#13137=EDGE_CURVE('',#10736,#10736,#9507,.T.);
#13138=EDGE_CURVE('',#10736,#10737,#5584,.T.);
#13139=EDGE_CURVE('',#10737,#10737,#9508,.T.);
#13140=EDGE_CURVE('',#10738,#10738,#9509,.T.);
#13141=EDGE_CURVE('',#10738,#10739,#5585,.T.);
#13142=EDGE_CURVE('',#10739,#10739,#9510,.T.);
#13143=EDGE_CURVE('',#10740,#10740,#9511,.T.);
#13144=EDGE_CURVE('',#10740,#10741,#5586,.T.);
#13145=EDGE_CURVE('',#10741,#10741,#9512,.T.);
#13146=EDGE_CURVE('',#10742,#10742,#9513,.T.);
#13147=EDGE_CURVE('',#10742,#10743,#5587,.T.);
#13148=EDGE_CURVE('',#10743,#10743,#9514,.T.);
#13149=EDGE_CURVE('',#10744,#10745,#5588,.T.);
#13150=EDGE_CURVE('',#10744,#10746,#9515,.T.);
#13151=EDGE_CURVE('',#10747,#10746,#5589,.T.);
#13152=EDGE_CURVE('',#10747,#10748,#5590,.T.);
#13153=EDGE_CURVE('',#10748,#10749,#5591,.T.);
#13154=EDGE_CURVE('',#10749,#10745,#9516,.T.);
#13155=EDGE_CURVE('',#10750,#10751,#5592,.T.);
#13156=EDGE_CURVE('',#10750,#10744,#5593,.T.);
#13157=EDGE_CURVE('',#10745,#10751,#5594,.T.);
#13158=EDGE_CURVE('',#10752,#10753,#5595,.T.);
#13159=EDGE_CURVE('',#10752,#10750,#9517,.T.);
#13160=EDGE_CURVE('',#10751,#10754,#9518,.T.);
#13161=EDGE_CURVE('',#10754,#10755,#5596,.T.);
#13162=EDGE_CURVE('',#10753,#10755,#5597,.T.);
#13163=EDGE_CURVE('',#10755,#10748,#5598,.T.);
#13164=EDGE_CURVE('',#10753,#10747,#5599,.T.);
#13165=EDGE_CURVE('',#10746,#10752,#5600,.T.);
#13166=EDGE_CURVE('',#10754,#10749,#5601,.T.);
#16870=ORIENTED_EDGE('',*,*,#13128,.F.);
#16871=ORIENTED_EDGE('',*,*,#13129,.T.);
#16872=ORIENTED_EDGE('',*,*,#13130,.T.);
#16873=ORIENTED_EDGE('',*,*,#13129,.F.);
#16874=ORIENTED_EDGE('',*,*,#13131,.F.);
#16875=ORIENTED_EDGE('',*,*,#13132,.T.);
#16876=ORIENTED_EDGE('',*,*,#13133,.T.);
#16877=ORIENTED_EDGE('',*,*,#13132,.F.);
#16878=ORIENTED_EDGE('',*,*,#13134,.F.);
#16879=ORIENTED_EDGE('',*,*,#13135,.T.);
#16880=ORIENTED_EDGE('',*,*,#13136,.T.);
#16881=ORIENTED_EDGE('',*,*,#13135,.F.);
#16882=ORIENTED_EDGE('',*,*,#13137,.F.);
#16883=ORIENTED_EDGE('',*,*,#13138,.T.);
#16884=ORIENTED_EDGE('',*,*,#13139,.T.);
#16885=ORIENTED_EDGE('',*,*,#13138,.F.);
#16886=ORIENTED_EDGE('',*,*,#13140,.F.);
#16887=ORIENTED_EDGE('',*,*,#13141,.T.);
#16888=ORIENTED_EDGE('',*,*,#13142,.T.);
#16889=ORIENTED_EDGE('',*,*,#13141,.F.);
#16890=ORIENTED_EDGE('',*,*,#13143,.F.);
#16891=ORIENTED_EDGE('',*,*,#13144,.T.);
#16892=ORIENTED_EDGE('',*,*,#13145,.T.);
#16893=ORIENTED_EDGE('',*,*,#13144,.F.);
#16894=ORIENTED_EDGE('',*,*,#13146,.F.);
#16895=ORIENTED_EDGE('',*,*,#13147,.T.);
#16896=ORIENTED_EDGE('',*,*,#13148,.T.);
#16897=ORIENTED_EDGE('',*,*,#13147,.F.);
#16898=ORIENTED_EDGE('',*,*,#13149,.F.);
#16899=ORIENTED_EDGE('',*,*,#13150,.T.);
#16900=ORIENTED_EDGE('',*,*,#13151,.F.);
#16901=ORIENTED_EDGE('',*,*,#13152,.T.);
#16902=ORIENTED_EDGE('',*,*,#13153,.T.);
#16903=ORIENTED_EDGE('',*,*,#13154,.T.);
#16904=ORIENTED_EDGE('',*,*,#13136,.F.);
#16905=ORIENTED_EDGE('',*,*,#13130,.F.);
#16906=ORIENTED_EDGE('',*,*,#13133,.F.);
#16907=ORIENTED_EDGE('',*,*,#13139,.F.);
#16908=ORIENTED_EDGE('',*,*,#13142,.F.);
#16909=ORIENTED_EDGE('',*,*,#13145,.F.);
#16910=ORIENTED_EDGE('',*,*,#13148,.F.);
#16911=ORIENTED_EDGE('',*,*,#13155,.F.);
#16912=ORIENTED_EDGE('',*,*,#13156,.T.);
#16913=ORIENTED_EDGE('',*,*,#13149,.T.);
#16914=ORIENTED_EDGE('',*,*,#13157,.T.);
#16915=ORIENTED_EDGE('',*,*,#13158,.F.);
#16916=ORIENTED_EDGE('',*,*,#13159,.T.);
#16917=ORIENTED_EDGE('',*,*,#13155,.T.);
#16918=ORIENTED_EDGE('',*,*,#13160,.T.);
#16919=ORIENTED_EDGE('',*,*,#13161,.T.);
#16920=ORIENTED_EDGE('',*,*,#13162,.F.);
#16921=ORIENTED_EDGE('',*,*,#13128,.T.);
#16922=ORIENTED_EDGE('',*,*,#13131,.T.);
#16923=ORIENTED_EDGE('',*,*,#13134,.T.);
#16924=ORIENTED_EDGE('',*,*,#13137,.T.);
#16925=ORIENTED_EDGE('',*,*,#13140,.T.);
#16926=ORIENTED_EDGE('',*,*,#13143,.T.);
#16927=ORIENTED_EDGE('',*,*,#13146,.T.);
#16928=ORIENTED_EDGE('',*,*,#13163,.T.);
#16929=ORIENTED_EDGE('',*,*,#13152,.F.);
#16930=ORIENTED_EDGE('',*,*,#13164,.F.);
#16931=ORIENTED_EDGE('',*,*,#13162,.T.);
#16932=ORIENTED_EDGE('',*,*,#13151,.T.);
#16933=ORIENTED_EDGE('',*,*,#13165,.T.);
#16934=ORIENTED_EDGE('',*,*,#13158,.T.);
#16935=ORIENTED_EDGE('',*,*,#13164,.T.);
#16936=ORIENTED_EDGE('',*,*,#13161,.F.);
#16937=ORIENTED_EDGE('',*,*,#13166,.T.);
#16938=ORIENTED_EDGE('',*,*,#13153,.F.);
#16939=ORIENTED_EDGE('',*,*,#13163,.F.);
#16940=ORIENTED_EDGE('',*,*,#13150,.F.);
#16941=ORIENTED_EDGE('',*,*,#13156,.F.);
#16942=ORIENTED_EDGE('',*,*,#13159,.F.);
#16943=ORIENTED_EDGE('',*,*,#13165,.F.);
#16944=ORIENTED_EDGE('',*,*,#13154,.F.);
#16945=ORIENTED_EDGE('',*,*,#13166,.F.);
#16946=ORIENTED_EDGE('',*,*,#13160,.F.);
#16947=ORIENTED_EDGE('',*,*,#13157,.F.);
#23822=CYLINDRICAL_SURFACE('',#26143,2.1);
#23823=CYLINDRICAL_SURFACE('',#26146,2.1);
#23824=CYLINDRICAL_SURFACE('',#26149,2.1);
#23825=CYLINDRICAL_SURFACE('',#26152,2.1);
#23826=CYLINDRICAL_SURFACE('',#26155,2.1);
#23827=CYLINDRICAL_SURFACE('',#26158,2.1);
#23828=CYLINDRICAL_SURFACE('',#26161,18.);
#23829=CYLINDRICAL_SURFACE('',#26174,10.);
#23830=CYLINDRICAL_SURFACE('',#26175,10.);
#24277=ADVANCED_FACE('',(#2324),#23822,.F.);
#24278=ADVANCED_FACE('',(#2325),#23823,.F.);
#24279=ADVANCED_FACE('',(#2326),#23824,.F.);
#24280=ADVANCED_FACE('',(#2327),#23825,.F.);
#24281=ADVANCED_FACE('',(#2328),#23826,.F.);
#24282=ADVANCED_FACE('',(#2329),#23827,.F.);
#24283=ADVANCED_FACE('',(#2330),#23828,.F.);
#24284=ADVANCED_FACE('',(#2331,#1209,#1210,#1211,#1212,#1213,#1214,#1215),
#1533,.F.);
#24285=ADVANCED_FACE('',(#2332),#1534,.F.);
#24286=ADVANCED_FACE('',(#2333,#1216,#1217,#1218,#1219,#1220,#1221,#1222),
#1535,.F.);
#24287=ADVANCED_FACE('',(#2334),#1536,.F.);
#24288=ADVANCED_FACE('',(#2335),#1537,.F.);
#24289=ADVANCED_FACE('',(#2336),#1538,.T.);
#24290=ADVANCED_FACE('',(#2337),#23829,.T.);
#24291=ADVANCED_FACE('',(#2338),#23830,.T.);
#25667=CLOSED_SHELL('',(#24277,#24278,#24279,#24280,#24281,#24282,#24283,
#24284,#24285,#24286,#24287,#24288,#24289,#24290,#24291));
#26142=AXIS2_PLACEMENT_3D('',#36466,#29056,#29057);
#26143=AXIS2_PLACEMENT_3D('',#36467,#29058,#29059);
#26144=AXIS2_PLACEMENT_3D('',#36469,#29060,#29061);
#26145=AXIS2_PLACEMENT_3D('',#36472,#29063,#29064);
#26146=AXIS2_PLACEMENT_3D('',#36473,#29065,#29066);
#26147=AXIS2_PLACEMENT_3D('',#36475,#29067,#29068);
#26148=AXIS2_PLACEMENT_3D('',#36478,#29070,#29071);
#26149=AXIS2_PLACEMENT_3D('',#36479,#29072,#29073);
#26150=AXIS2_PLACEMENT_3D('',#36481,#29074,#29075);
#26151=AXIS2_PLACEMENT_3D('',#36484,#29077,#29078);
#26152=AXIS2_PLACEMENT_3D('',#36485,#29079,#29080);
#26153=AXIS2_PLACEMENT_3D('',#36487,#29081,#29082);
#26154=AXIS2_PLACEMENT_3D('',#36490,#29084,#29085);
#26155=AXIS2_PLACEMENT_3D('',#36491,#29086,#29087);
#26156=AXIS2_PLACEMENT_3D('',#36493,#29088,#29089);
#26157=AXIS2_PLACEMENT_3D('',#36496,#29091,#29092);
#26158=AXIS2_PLACEMENT_3D('',#36497,#29093,#29094);
#26159=AXIS2_PLACEMENT_3D('',#36499,#29095,#29096);
#26160=AXIS2_PLACEMENT_3D('',#36502,#29098,#29099);
#26161=AXIS2_PLACEMENT_3D('',#36503,#29100,#29101);
#26162=AXIS2_PLACEMENT_3D('',#36505,#29102,#29103);
#26163=AXIS2_PLACEMENT_3D('',#36508,#29105,#29106);
#26164=AXIS2_PLACEMENT_3D('',#36509,#29107,#29108);
#26165=AXIS2_PLACEMENT_3D('',#36514,#29110,#29111);
#26166=AXIS2_PLACEMENT_3D('',#36521,#29115,#29116);
#26167=AXIS2_PLACEMENT_3D('',#36522,#29117,#29118);
#26168=AXIS2_PLACEMENT_3D('',#36528,#29122,#29123);
#26169=AXIS2_PLACEMENT_3D('',#36532,#29125,#29126);
#26170=AXIS2_PLACEMENT_3D('',#36534,#29127,#29128);
#26171=AXIS2_PLACEMENT_3D('',#36538,#29131,#29132);
#26172=AXIS2_PLACEMENT_3D('',#36541,#29135,#29136);
#26173=AXIS2_PLACEMENT_3D('',#36543,#29138,#29139);
#26174=AXIS2_PLACEMENT_3D('',#36545,#29141,#29142);
#26175=AXIS2_PLACEMENT_3D('',#36546,#29143,#29144);
#29056=DIRECTION('axis',(0.,0.,1.));
#29057=DIRECTION('refdir',(1.,0.,0.));
#29058=DIRECTION('center_axis',(0.,-1.,0.));
#29059=DIRECTION('ref_axis',(0.,0.,-1.));
#29060=DIRECTION('center_axis',(0.,-1.,0.));
#29061=DIRECTION('ref_axis',(0.,0.,-1.));
#29062=DIRECTION('',(0.,-1.,0.));
#29063=DIRECTION('center_axis',(0.,-1.,0.));
#29064=DIRECTION('ref_axis',(0.,0.,-1.));
#29065=DIRECTION('center_axis',(0.,-1.,0.));
#29066=DIRECTION('ref_axis',(0.,0.,-1.));
#29067=DIRECTION('center_axis',(0.,-1.,0.));
#29068=DIRECTION('ref_axis',(0.,0.,-1.));
#29069=DIRECTION('',(0.,-1.,0.));
#29070=DIRECTION('center_axis',(0.,-1.,0.));
#29071=DIRECTION('ref_axis',(0.,0.,-1.));
#29072=DIRECTION('center_axis',(0.,-1.,0.));
#29073=DIRECTION('ref_axis',(0.,0.,-1.));
#29074=DIRECTION('center_axis',(0.,-1.,0.));
#29075=DIRECTION('ref_axis',(0.,0.,-1.));
#29076=DIRECTION('',(0.,-1.,0.));
#29077=DIRECTION('center_axis',(0.,-1.,0.));
#29078=DIRECTION('ref_axis',(0.,0.,-1.));
#29079=DIRECTION('center_axis',(0.,-1.,0.));
#29080=DIRECTION('ref_axis',(0.,0.,-1.));
#29081=DIRECTION('center_axis',(0.,-1.,0.));
#29082=DIRECTION('ref_axis',(0.,0.,-1.));
#29083=DIRECTION('',(0.,-1.,0.));
#29084=DIRECTION('center_axis',(0.,-1.,0.));
#29085=DIRECTION('ref_axis',(0.,0.,-1.));
#29086=DIRECTION('center_axis',(0.,-1.,0.));
#29087=DIRECTION('ref_axis',(0.,0.,-1.));
#29088=DIRECTION('center_axis',(0.,-1.,0.));
#29089=DIRECTION('ref_axis',(0.,0.,-1.));
#29090=DIRECTION('',(0.,-1.,0.));
#29091=DIRECTION('center_axis',(0.,-1.,0.));
#29092=DIRECTION('ref_axis',(0.,0.,-1.));
#29093=DIRECTION('center_axis',(0.,-1.,0.));
#29094=DIRECTION('ref_axis',(0.,0.,-1.));
#29095=DIRECTION('center_axis',(0.,-1.,0.));
#29096=DIRECTION('ref_axis',(0.,0.,-1.));
#29097=DIRECTION('',(0.,-1.,0.));
#29098=DIRECTION('center_axis',(0.,-1.,0.));
#29099=DIRECTION('ref_axis',(0.,0.,-1.));
#29100=DIRECTION('center_axis',(0.,-1.,0.));
#29101=DIRECTION('ref_axis',(0.,0.,-1.));
#29102=DIRECTION('center_axis',(0.,-1.,0.));
#29103=DIRECTION('ref_axis',(0.,0.,-1.));
#29104=DIRECTION('',(0.,-1.,0.));
#29105=DIRECTION('center_axis',(0.,-1.,0.));
#29106=DIRECTION('ref_axis',(0.,0.,-1.));
#29107=DIRECTION('center_axis',(0.,1.,0.));
#29108=DIRECTION('ref_axis',(0.,0.,1.));
#29109=DIRECTION('',(0.,0.,-1.));
#29110=DIRECTION('center_axis',(0.,-1.,0.));
#29111=DIRECTION('ref_axis',(0.,0.,1.));
#29112=DIRECTION('',(1.,0.,0.));
#29113=DIRECTION('',(0.,0.,-1.));
#29114=DIRECTION('',(1.,0.,0.));
#29115=DIRECTION('center_axis',(0.,-1.,0.));
#29116=DIRECTION('ref_axis',(0.,0.,1.));
#29117=DIRECTION('center_axis',(-1.,0.,0.));
#29118=DIRECTION('ref_axis',(0.,0.,1.));
#29119=DIRECTION('',(0.,0.,-1.));
#29120=DIRECTION('',(0.,-1.,0.));
#29121=DIRECTION('',(0.,1.,0.));
#29122=DIRECTION('center_axis',(0.,-1.,0.));
#29123=DIRECTION('ref_axis',(0.,0.,-1.));
#29124=DIRECTION('',(-1.,0.,0.));
#29125=DIRECTION('center_axis',(0.,1.,0.));
#29126=DIRECTION('ref_axis',(0.,0.,-1.));
#29127=DIRECTION('center_axis',(0.,1.,0.));
#29128=DIRECTION('ref_axis',(0.,0.,-1.));
#29129=DIRECTION('',(-1.,0.,0.));
#29130=DIRECTION('',(0.,0.,-1.));
#29131=DIRECTION('center_axis',(1.,0.,0.));
#29132=DIRECTION('ref_axis',(0.,0.,-1.));
#29133=DIRECTION('',(0.,-1.,0.));
#29134=DIRECTION('',(0.,-1.,0.));
#29135=DIRECTION('center_axis',(0.,0.,-1.));
#29136=DIRECTION('ref_axis',(-1.,0.,0.));
#29137=DIRECTION('',(0.,1.,0.));
#29138=DIRECTION('center_axis',(0.,0.,-1.));
#29139=DIRECTION('ref_axis',(-1.,0.,0.));
#29140=DIRECTION('',(0.,-1.,0.));
#29141=DIRECTION('center_axis',(0.,1.,0.));
#29142=DIRECTION('ref_axis',(0.,0.,1.));
#29143=DIRECTION('center_axis',(0.,-1.,0.));
#29144=DIRECTION('ref_axis',(0.,0.,-1.));
#36466=CARTESIAN_POINT('',(0.,0.,0.));
#36467=CARTESIAN_POINT('Origin',(-6.61700935788389,-7.,16.6170093578838));
#36468=CARTESIAN_POINT('',(-6.61700935788389,7.,18.7170093578838));
#36469=CARTESIAN_POINT('Origin',(-6.61700935788389,7.,16.6170093578838));
#36470=CARTESIAN_POINT('',(-6.61700935788389,-7.,18.7170093578838));
#36471=CARTESIAN_POINT('',(-6.61700935788389,-7.,18.7170093578838));
#36472=CARTESIAN_POINT('Origin',(-6.61700935788389,-7.,16.6170093578838));
#36473=CARTESIAN_POINT('Origin',(10.,-7.,23.5));
#36474=CARTESIAN_POINT('',(10.,7.,25.6));
#36475=CARTESIAN_POINT('Origin',(10.,7.,23.5));
#36476=CARTESIAN_POINT('',(10.,-7.,25.6));
#36477=CARTESIAN_POINT('',(10.,-7.,25.6));
#36478=CARTESIAN_POINT('Origin',(10.,-7.,23.5));
#36479=CARTESIAN_POINT('Origin',(26.6170093578838,-7.,16.617009357884));
#36480=CARTESIAN_POINT('',(26.6170093578838,7.,18.7170093578839));
#36481=CARTESIAN_POINT('Origin',(26.6170093578838,7.,16.617009357884));
#36482=CARTESIAN_POINT('',(26.6170093578838,-7.,18.7170093578839));
#36483=CARTESIAN_POINT('',(26.6170093578838,-7.,18.7170093578839));
#36484=CARTESIAN_POINT('Origin',(26.6170093578838,-7.,16.617009357884));
#36485=CARTESIAN_POINT('Origin',(-6.61700935788389,-7.,-16.6170093578838));
#36486=CARTESIAN_POINT('',(-6.61700935788389,7.,-14.5170093578838));
#36487=CARTESIAN_POINT('Origin',(-6.61700935788389,7.,-16.6170093578838));
#36488=CARTESIAN_POINT('',(-6.61700935788389,-7.,-14.5170093578838));
#36489=CARTESIAN_POINT('',(-6.61700935788389,-7.,-14.5170093578838));
#36490=CARTESIAN_POINT('Origin',(-6.61700935788389,-7.,-16.6170093578838));
#36491=CARTESIAN_POINT('Origin',(10.,-7.,-23.5));
#36492=CARTESIAN_POINT('',(10.,7.,-21.4));
#36493=CARTESIAN_POINT('Origin',(10.,7.,-23.5));
#36494=CARTESIAN_POINT('',(10.,-7.,-21.4));
#36495=CARTESIAN_POINT('',(10.,-7.,-21.4));
#36496=CARTESIAN_POINT('Origin',(10.,-7.,-23.5));
#36497=CARTESIAN_POINT('Origin',(26.6170093578838,-7.,-16.617009357884));
#36498=CARTESIAN_POINT('',(26.6170093578838,7.,-14.517009357884));
#36499=CARTESIAN_POINT('Origin',(26.6170093578838,7.,-16.617009357884));
#36500=CARTESIAN_POINT('',(26.6170093578838,-7.,-14.517009357884));
#36501=CARTESIAN_POINT('',(26.6170093578838,-7.,-14.517009357884));
#36502=CARTESIAN_POINT('Origin',(26.6170093578838,-7.,-16.617009357884));
#36503=CARTESIAN_POINT('Origin',(10.,7.,0.));
#36504=CARTESIAN_POINT('',(10.,7.,18.));
#36505=CARTESIAN_POINT('Origin',(10.,7.,0.));
#36506=CARTESIAN_POINT('',(10.,-7.,18.));
#36507=CARTESIAN_POINT('',(10.,7.,18.));
#36508=CARTESIAN_POINT('Origin',(10.,-7.,0.));
#36509=CARTESIAN_POINT('Origin',(-32.,-7.,27.5));
#36510=CARTESIAN_POINT('',(32.,-7.,17.5));
#36511=CARTESIAN_POINT('',(32.,-7.,-17.5));
#36512=CARTESIAN_POINT('',(32.,-7.,27.5));
#36513=CARTESIAN_POINT('',(22.,-7.,27.5));
#36514=CARTESIAN_POINT('Origin',(22.,-7.,17.5));
#36515=CARTESIAN_POINT('',(-32.,-7.,27.5));
#36516=CARTESIAN_POINT('',(-32.,-7.,27.5));
#36517=CARTESIAN_POINT('',(-32.,-7.,-27.5));
#36518=CARTESIAN_POINT('',(-32.,-7.,27.5));
#36519=CARTESIAN_POINT('',(22.,-7.,-27.5));
#36520=CARTESIAN_POINT('',(-32.,-7.,-27.5));
#36521=CARTESIAN_POINT('Origin',(22.,-7.,-17.5));
#36522=CARTESIAN_POINT('Origin',(32.,-7.,27.5));
#36523=CARTESIAN_POINT('',(32.,7.,17.5));
#36524=CARTESIAN_POINT('',(32.,7.,-17.5));
#36525=CARTESIAN_POINT('',(32.,7.,27.5));
#36526=CARTESIAN_POINT('',(32.,-7.,17.5));
#36527=CARTESIAN_POINT('',(32.,7.,-17.5));
#36528=CARTESIAN_POINT('Origin',(-32.,7.,27.5));
#36529=CARTESIAN_POINT('',(22.,7.,27.5));
#36530=CARTESIAN_POINT('',(-32.,7.,27.5));
#36531=CARTESIAN_POINT('',(-32.,7.,27.5));
#36532=CARTESIAN_POINT('Origin',(22.,7.,17.5));
#36533=CARTESIAN_POINT('',(22.,7.,-27.5));
#36534=CARTESIAN_POINT('Origin',(22.,7.,-17.5));
#36535=CARTESIAN_POINT('',(-32.,7.,-27.5));
#36536=CARTESIAN_POINT('',(-32.,7.,-27.5));
#36537=CARTESIAN_POINT('',(-32.,7.,27.5));
#36538=CARTESIAN_POINT('Origin',(-32.,-7.,27.5));
#36539=CARTESIAN_POINT('',(-32.,-7.,-27.5));
#36540=CARTESIAN_POINT('',(-32.,-7.,27.5));
#36541=CARTESIAN_POINT('Origin',(0.,0.,27.5));
#36542=CARTESIAN_POINT('',(22.,0.,27.5));
#36543=CARTESIAN_POINT('Origin',(0.,0.,-27.5));
#36544=CARTESIAN_POINT('',(22.,-7.,-27.5));
#36545=CARTESIAN_POINT('Origin',(22.,0.,17.5));
#36546=CARTESIAN_POINT('Origin',(22.,-7.,-17.5));
#66646=UNCERTAINTY_MEASURE_WITH_UNIT(LENGTH_MEASURE(0.01),#66722,
'DISTANCE_ACCURACY_VALUE',
'Maximum model space distance between geometric entities at asserted c
onnectivities');
#66680=UNCERTAINTY_MEASURE_WITH_UNIT(LENGTH_MEASURE(0.01),#66722,
'DISTANCE_ACCURACY_VALUE',
'Maximum model space distance between geometric entities at asserted c
onnectivities');
#66687=(
GEOMETRIC_REPRESENTATION_CONTEXT(3)
GLOBAL_UNCERTAINTY_ASSIGNED_CONTEXT((#66646))
GLOBAL_UNIT_ASSIGNED_CONTEXT((#66722,#66724,#66725))
REPRESENTATION_CONTEXT('','3D')
);
#66721=(
GEOMETRIC_REPRESENTATION_CONTEXT(3)
GLOBAL_UNCERTAINTY_ASSIGNED_CONTEXT((#66680))
GLOBAL_UNIT_ASSIGNED_CONTEXT((#66722,#66724,#66725))
REPRESENTATION_CONTEXT('','3D')
);
#66722=(
LENGTH_UNIT()
NAMED_UNIT(*)
SI_UNIT(.MILLI.,.METRE.)
);
#66724=(
NAMED_UNIT(*)
PLANE_ANGLE_UNIT()
SI_UNIT($,.RADIAN.)
);
#66725=(
NAMED_UNIT(*)
SI_UNIT($,.STERADIAN.)
SOLID_ANGLE_UNIT()
);
#66732=SHAPE_DEFINITION_REPRESENTATION(#66772,#66896);
#66772=PRODUCT_DEFINITION_SHAPE('',$,#66937);
#66896=SHAPE_REPRESENTATION('',(#26142),#66687);
#66930=PRODUCT_DEFINITION_CONTEXT('part definition',#67052,'design');
#66937=PRODUCT_DEFINITION('Ball Screw Support Bracket',
'Ball Screw Support Bracket',#66977,#66930);
#66977=PRODUCT_DEFINITION_FORMATION('',$,#67060);
#67052=APPLICATION_CONTEXT(
'Core Data for Automotive Mechanical Design Process');
#67053=PRODUCT_CONTEXT('part definition',#67052,'mechanical');
#67060=PRODUCT('Ball Screw Support Bracket',
'Ball Screw Support Bracket',$,(#67053));
#67095=PRESENTATION_STYLE_ASSIGNMENT((#67097));
#67097=SURFACE_STYLE_USAGE(.BOTH.,#67099);
#67099=SURFACE_SIDE_STYLE('',(#67101));
#67101=SURFACE_STYLE_FILL_AREA(#67103);
#67103=FILL_AREA_STYLE('Opaque(202,209,238)',(#67105));
#67105=FILL_AREA_STYLE_COLOUR('Opaque(202,209,238)',#67107);
#67107=COLOUR_RGB('Opaque(202,209,238)',0.792156862745098,0.819607843137255,
0.933333333333333);
ENDSEC;
END-ISO-10303-21;
